ISO-10303-21;
HEADER;
/* Generated by software containing ST-Developer
 * from STEP Tools, Inc. (www.steptools.com) 
 */

FILE_DESCRIPTION(
/* description */ ('Grid plate located blocks and clamp'),
/* implementation_level */ '2;1');

FILE_NAME(
/* name */ 'Flat Washer - M8.step',
/* time_stamp */ '2026-10-29T15:43:47-07:00',
/* author */ (''),
/* organization */ (''),
/* preprocessor_version */ 'ST-DEVELOPER v20.2',
/* originating_system */ 'Autodesk Translation Framework v15.17.0.0',
/* authorisation */ '');

FILE_SCHEMA (('AUTOMOTIVE_DESIGN { 1 0 10303 214 3 1 1 }'));
ENDSEC;

DATA;
#10=MECHANICAL_DESIGN_GEOMETRIC_PRESENTATION_REPRESENTATION('',(#177),#5702);
#151=SHAPE_REPRESENTATION_RELATIONSHIP('SRR','None',#5769,#163);
#163=ADVANCED_BREP_SHAPE_REPRESENTATION('',(#189),#5699);
#177=STYLED_ITEM('',(#5904),#189);
#189=MANIFOLD_SOLID_BREP('Body1',#3274);
#261=FACE_BOUND('',#858,.T.);
#262=FACE_BOUND('',#860,.T.);
#363=CIRCLE('',#3665,0.42);
#364=CIRCLE('',#3666,0.42);
#365=CIRCLE('',#3668,0.8);
#366=CIRCLE('',#3669,0.8);
#441=CYLINDRICAL_SURFACE('',#3664,0.42);
#442=CYLINDRICAL_SURFACE('',#3667,0.8);
#603=FACE_OUTER_BOUND('',#855,.T.);
#604=FACE_OUTER_BOUND('',#856,.T.);
#605=FACE_OUTER_BOUND('',#857,.T.);
#606=FACE_OUTER_BOUND('',#859,.T.);
#855=EDGE_LOOP('',(#2788,#2789,#2790,#2791));
#856=EDGE_LOOP('',(#2792,#2793,#2794,#2795));
#857=EDGE_LOOP('',(#2796));
#858=EDGE_LOOP('',(#2797));
#859=EDGE_LOOP('',(#2798));
#860=EDGE_LOOP('',(#2799));
#1130=LINE('',#5444,#1403);
#1131=LINE('',#5450,#1404);
#1403=VECTOR('',#4506,0.42);
#1404=VECTOR('',#4513,0.8);
#1658=VERTEX_POINT('',#5441);
#1659=VERTEX_POINT('',#5443);
#1660=VERTEX_POINT('',#5447);
#1661=VERTEX_POINT('',#5449);
#2044=EDGE_CURVE('',#1658,#1658,#363,.T.);
#2045=EDGE_CURVE('',#1658,#1659,#1130,.T.);
#2046=EDGE_CURVE('',#1659,#1659,#364,.T.);
#2047=EDGE_CURVE('',#1660,#1660,#365,.T.);
#2048=EDGE_CURVE('',#1660,#1661,#1131,.T.);
#2049=EDGE_CURVE('',#1661,#1661,#366,.T.);
#2788=ORIENTED_EDGE('',*,*,#2044,.F.);
#2789=ORIENTED_EDGE('',*,*,#2045,.T.);
#2790=ORIENTED_EDGE('',*,*,#2046,.T.);
#2791=ORIENTED_EDGE('',*,*,#2045,.F.);
#2792=ORIENTED_EDGE('',*,*,#2047,.F.);
#2793=ORIENTED_EDGE('',*,*,#2048,.T.);
#2794=ORIENTED_EDGE('',*,*,#2049,.T.);
#2795=ORIENTED_EDGE('',*,*,#2048,.F.);
#2796=ORIENTED_EDGE('',*,*,#2047,.T.);
#2797=ORIENTED_EDGE('',*,*,#2044,.T.);
#2798=ORIENTED_EDGE('',*,*,#2049,.F.);
#2799=ORIENTED_EDGE('',*,*,#2046,.F.);
#3059=PLANE('',#3670);
#3060=PLANE('',#3671);
#3224=ADVANCED_FACE('',(#603),#441,.F.);
#3225=ADVANCED_FACE('',(#604),#442,.T.);
#3226=ADVANCED_FACE('',(#605,#261),#3059,.T.);
#3227=ADVANCED_FACE('',(#606,#262),#3060,.F.);
#3274=CLOSED_SHELL('',(#3224,#3225,#3226,#3227));
#3663=AXIS2_PLACEMENT_3D('',#5439,#4500,#4501);
#3664=AXIS2_PLACEMENT_3D('',#5440,#4502,#4503);
#3665=AXIS2_PLACEMENT_3D('',#5442,#4504,#4505);
#3666=AXIS2_PLACEMENT_3D('',#5445,#4507,#4508);
#3667=AXIS2_PLACEMENT_3D('',#5446,#4509,#4510);
#3668=AXIS2_PLACEMENT_3D('',#5448,#4511,#4512);
#3669=AXIS2_PLACEMENT_3D('',#5451,#4514,#4515);
#3670=AXIS2_PLACEMENT_3D('',#5452,#4516,#4517);
#3671=AXIS2_PLACEMENT_3D('',#5453,#4518,#4519);
#4500=DIRECTION('axis',(0.,0.,1.));
#4501=DIRECTION('refdir',(1.,0.,0.));
#4502=DIRECTION('center_axis',(0.,1.,0.));
#4503=DIRECTION('ref_axis',(1.,0.,0.));
#4504=DIRECTION('center_axis',(0.,-1.,0.));
#4505=DIRECTION('ref_axis',(1.,0.,0.));
#4506=DIRECTION('',(0.,-1.,0.));
#4507=DIRECTION('center_axis',(0.,-1.,0.));
#4508=DIRECTION('ref_axis',(1.,0.,0.));
#4509=DIRECTION('center_axis',(0.,1.,0.));
#4510=DIRECTION('ref_axis',(1.,0.,0.));
#4511=DIRECTION('center_axis',(0.,1.,0.));
#4512=DIRECTION('ref_axis',(1.,0.,0.));
#4513=DIRECTION('',(0.,-1.,0.));
#4514=DIRECTION('center_axis',(0.,1.,0.));
#4515=DIRECTION('ref_axis',(1.,0.,0.));
#4516=DIRECTION('center_axis',(0.,1.,0.));
#4517=DIRECTION('ref_axis',(1.,0.,0.));
#4518=DIRECTION('center_axis',(0.,1.,0.));
#4519=DIRECTION('ref_axis',(1.,0.,0.));
#5439=CARTESIAN_POINT('',(0.,0.,0.));
#5440=CARTESIAN_POINT('Origin',(0.,0.,0.));
#5441=CARTESIAN_POINT('',(-0.42,0.16,5.14351655641888E-17));
#5442=CARTESIAN_POINT('Origin',(0.,0.16,0.));
#5443=CARTESIAN_POINT('',(-0.42,0.,5.14351655641888E-17));
#5444=CARTESIAN_POINT('',(-0.42,0.,5.14351655641888E-17));
#5445=CARTESIAN_POINT('Origin',(0.,0.,0.));
#5446=CARTESIAN_POINT('Origin',(0.,0.,0.));
#5447=CARTESIAN_POINT('',(-0.8,0.16,9.79717439317883E-17));
#5448=CARTESIAN_POINT('Origin',(0.,0.16,0.));
#5449=CARTESIAN_POINT('',(-0.8,0.,9.79717439317883E-17));
#5450=CARTESIAN_POINT('',(-0.8,0.,9.79717439317883E-17));
#5451=CARTESIAN_POINT('Origin',(0.,0.,0.));
#5452=CARTESIAN_POINT('Origin',(0.,0.16,0.));
#5453=CARTESIAN_POINT('Origin',(0.,0.,0.));
#5685=UNCERTAINTY_MEASURE_WITH_UNIT(LENGTH_MEASURE(0.001),#5703,
'DISTANCE_ACCURACY_VALUE',
'Maximum model space distance between geometric entities at asserted c
onnectivities');
#5688=UNCERTAINTY_MEASURE_WITH_UNIT(LENGTH_MEASURE(0.001),#5703,
'DISTANCE_ACCURACY_VALUE',
'Maximum model space distance between geometric entities at asserted c
onnectivities');
#5699=(
GEOMETRIC_REPRESENTATION_CONTEXT(3)
GLOBAL_UNCERTAINTY_ASSIGNED_CONTEXT((#5685))
GLOBAL_UNIT_ASSIGNED_CONTEXT((#5703,#5705,#5706))
REPRESENTATION_CONTEXT('','3D')
);
#5702=(
GEOMETRIC_REPRESENTATION_CONTEXT(3)
GLOBAL_UNCERTAINTY_ASSIGNED_CONTEXT((#5688))
GLOBAL_UNIT_ASSIGNED_CONTEXT((#5703,#5705,#5706))
REPRESENTATION_CONTEXT('','3D')
);
#5703=(
LENGTH_UNIT()
NAMED_UNIT(*)
SI_UNIT(.CENTI.,.METRE.)
);
#5705=(
NAMED_UNIT(*)
PLANE_ANGLE_UNIT()
SI_UNIT($,.RADIAN.)
);
#5706=(
NAMED_UNIT(*)
SI_UNIT($,.STERADIAN.)
SOLID_ANGLE_UNIT()
);
#5717=SHAPE_DEFINITION_REPRESENTATION(#5730,#5769);
#5730=PRODUCT_DEFINITION_SHAPE('',$,#5783);
#5769=SHAPE_REPRESENTATION('',(#3663),#5699);
#5772=PRODUCT_DEFINITION_CONTEXT('part definition',#5813,'design');
#5783=PRODUCT_DEFINITION('Flat Washer - M8','Flat Washer - M8',
#5796,#5772);
#5796=PRODUCT_DEFINITION_FORMATION('',$,#5825);
#5813=APPLICATION_CONTEXT(
'Core Data for Automotive Mechanical Design Process');
#5814=PRODUCT_CONTEXT('part definition',#5813,'mechanical');
#5825=PRODUCT('Flat Washer - M8','Flat Washer - M8',
'Flat Washer - M8',(#5814));
#5898=COLOUR_RGB('Black',0.12,0.14,0.17);
#5899=FILL_AREA_STYLE_COLOUR('',#5898);
#5900=FILL_AREA_STYLE('',(#5899));
#5901=SURFACE_STYLE_FILL_AREA(#5900);
#5902=SURFACE_SIDE_STYLE('',(#5901));
#5903=SURFACE_STYLE_USAGE(.BOTH.,#5902);
#5904=PRESENTATION_STYLE_ASSIGNMENT((#5903));
ENDSEC;
END-ISO-10303-21;
